ISO-10303-21;
HEADER;
/* Generated by software containing ST-Developer
 * from STEP Tools, Inc. (www.steptools.com) 
 */

FILE_DESCRIPTION(
/* description */ (''),
/* implementation_level */ '2;1');

FILE_NAME(
/* name */ 'Ring_02.step',
/* time_stamp */ '2026-10-06T13:15:55-07:00',
/* author */ (''),
/* organization */ (''),
/* preprocessor_version */ 'ST-DEVELOPER v20.2',
/* originating_system */ 'Autodesk Translation Framework v15.15.0.0',
/* authorisation */ '');

FILE_SCHEMA (('AUTOMOTIVE_DESIGN { 1 0 10303 214 3 1 1 }'));
ENDSEC;

DATA;
#10=MECHANICAL_DESIGN_GEOMETRIC_PRESENTATION_REPRESENTATION('',(#115),#27707);
#53=TOROIDAL_SURFACE('',#4145,6.10923539706593,0.3);
#54=TOROIDAL_SURFACE('',#4152,6.1088989677085,0.3);
#82=CONICAL_SURFACE('',#4149,6.40906719549494,0.00029560929023293);
#95=SHAPE_REPRESENTATION_RELATIONSHIP('SRR','None',#27752,#105);
#105=ADVANCED_BREP_SHAPE_REPRESENTATION('',(#125),#27704);
#115=STYLED_ITEM('',(#27804),#125);
#125=MANIFOLD_SOLID_BREP('Body1',#3841);
#201=PLANE('',#4151);
#202=PLANE('',#4155);
#285=CIRCLE('',#4146,6.10923539706593);
#286=CIRCLE('',#4147,0.3);
#287=CIRCLE('',#4148,6.4092353839582);
#288=CIRCLE('',#4150,6.40889895460077);
#289=CIRCLE('',#4153,0.3);
#290=CIRCLE('',#4154,6.1088989677085);
#585=FACE_OUTER_BOUND('',#829,.T.);
#586=FACE_OUTER_BOUND('',#830,.T.);
#587=FACE_OUTER_BOUND('',#831,.T.);
#588=FACE_OUTER_BOUND('',#832,.T.);
#589=FACE_OUTER_BOUND('',#833,.T.);
#829=EDGE_LOOP('',(#3219,#3220,#3221,#3222));
#830=EDGE_LOOP('',(#3223,#3224,#3225,#3226));
#831=EDGE_LOOP('',(#3227));
#832=EDGE_LOOP('',(#3228,#3229,#3230,#3231));
#833=EDGE_LOOP('',(#3232));
#1051=LINE('',#15710,#1227);
#1227=VECTOR('',#4814,6.40906719549494);
#1778=VERTEX_POINT('',#15703);
#1779=VERTEX_POINT('',#15705);
#1780=VERTEX_POINT('',#15709);
#1781=VERTEX_POINT('',#15714);
#2279=EDGE_CURVE('',#1778,#1778,#285,.T.);
#2280=EDGE_CURVE('',#1778,#1779,#286,.T.);
#2281=EDGE_CURVE('',#1779,#1779,#287,.T.);
#2282=EDGE_CURVE('',#1779,#1780,#1051,.T.);
#2283=EDGE_CURVE('',#1780,#1780,#288,.T.);
#2284=EDGE_CURVE('',#1780,#1781,#289,.T.);
#2285=EDGE_CURVE('',#1781,#1781,#290,.T.);
#3219=ORIENTED_EDGE('',*,*,#2279,.T.);
#3220=ORIENTED_EDGE('',*,*,#2280,.T.);
#3221=ORIENTED_EDGE('',*,*,#2281,.T.);
#3222=ORIENTED_EDGE('',*,*,#2280,.F.);
#3223=ORIENTED_EDGE('',*,*,#2281,.F.);
#3224=ORIENTED_EDGE('',*,*,#2282,.T.);
#3225=ORIENTED_EDGE('',*,*,#2283,.F.);
#3226=ORIENTED_EDGE('',*,*,#2282,.F.);
#3227=ORIENTED_EDGE('',*,*,#2279,.F.);
#3228=ORIENTED_EDGE('',*,*,#2283,.T.);
#3229=ORIENTED_EDGE('',*,*,#2284,.T.);
#3230=ORIENTED_EDGE('',*,*,#2285,.T.);
#3231=ORIENTED_EDGE('',*,*,#2284,.F.);
#3232=ORIENTED_EDGE('',*,*,#2285,.F.);
#3760=ADVANCED_FACE('',(#585),#53,.T.);
#3761=ADVANCED_FACE('',(#586),#82,.T.);
#3762=ADVANCED_FACE('',(#587),#201,.T.);
#3763=ADVANCED_FACE('',(#588),#54,.T.);
#3764=ADVANCED_FACE('',(#589),#202,.T.);
#3841=CLOSED_SHELL('',(#3760,#3761,#3762,#3763,#3764));
#4144=AXIS2_PLACEMENT_3D('',#15701,#4802,#4803);
#4145=AXIS2_PLACEMENT_3D('',#15702,#4804,#4805);
#4146=AXIS2_PLACEMENT_3D('',#15704,#4806,#4807);
#4147=AXIS2_PLACEMENT_3D('',#15706,#4808,#4809);
#4148=AXIS2_PLACEMENT_3D('',#15707,#4810,#4811);
#4149=AXIS2_PLACEMENT_3D('',#15708,#4812,#4813);
#4150=AXIS2_PLACEMENT_3D('',#15711,#4815,#4816);
#4151=AXIS2_PLACEMENT_3D('',#15712,#4817,#4818);
#4152=AXIS2_PLACEMENT_3D('',#15713,#4819,#4820);
#4153=AXIS2_PLACEMENT_3D('',#15715,#4821,#4822);
#4154=AXIS2_PLACEMENT_3D('',#15716,#4823,#4824);
#4155=AXIS2_PLACEMENT_3D('',#15717,#4825,#4826);
#4802=DIRECTION('axis',(0.,0.,1.));
#4803=DIRECTION('refdir',(1.,0.,0.));
#4804=DIRECTION('center_axis',(1.,0.,0.));
#4805=DIRECTION('ref_axis',(0.,0.,-1.));
#4806=DIRECTION('center_axis',(-1.,0.,0.));
#4807=DIRECTION('ref_axis',(0.,1.22464679914735E-16,1.));
#4808=DIRECTION('center_axis',(0.,-1.,-1.22464679914735E-16));
#4809=DIRECTION('ref_axis',(0.,-1.22464679914735E-16,1.));
#4810=DIRECTION('center_axis',(1.,0.,0.));
#4811=DIRECTION('ref_axis',(0.,0.,1.));
#4812=DIRECTION('center_axis',(1.,0.,0.));
#4813=DIRECTION('ref_axis',(0.,0.,-1.));
#4814=DIRECTION('',(-0.999999956307574,3.62016965809512E-20,-0.000295609285927634));
#4815=DIRECTION('center_axis',(-1.,0.,0.));
#4816=DIRECTION('ref_axis',(0.,0.,1.));
#4817=DIRECTION('center_axis',(1.,0.,0.));
#4818=DIRECTION('ref_axis',(0.,0.,-1.));
#4819=DIRECTION('center_axis',(1.,0.,0.));
#4820=DIRECTION('ref_axis',(0.,0.,-1.));
#4821=DIRECTION('center_axis',(0.,-1.,-1.22464679914735E-16));
#4822=DIRECTION('ref_axis',(0.,-1.22464679914735E-16,1.));
#4823=DIRECTION('center_axis',(1.,0.,0.));
#4824=DIRECTION('ref_axis',(0.,1.22464679914735E-16,1.));
#4825=DIRECTION('center_axis',(-1.,0.,0.));
#4826=DIRECTION('ref_axis',(0.,0.,1.));
#15701=CARTESIAN_POINT('',(0.,0.,0.));
#15702=CARTESIAN_POINT('Origin',(30.1110679337117,0.,0.));
#15703=CARTESIAN_POINT('',(30.4110679337117,-7.4816555742545E-16,6.10923539706593));
#15704=CARTESIAN_POINT('Origin',(30.4110679337117,0.,0.));
#15705=CARTESIAN_POINT('',(30.1109792509259,-7.84904959794637E-16,6.4092353839582));
#15706=CARTESIAN_POINT('Origin',(30.1110679337117,-7.4816555742545E-16,
6.10923539706593));
#15707=CARTESIAN_POINT('Origin',(30.1109792509259,-7.84904959794637E-16,
0.));
#15708=CARTESIAN_POINT('Origin',(29.5420239984498,0.,0.));
#15709=CARTESIAN_POINT('',(28.9728913804021,-7.84863759081066E-16,6.40889895460077));
#15710=CARTESIAN_POINT('',(29.5420239984498,-7.84884362648318E-16,6.40906719549494));
#15711=CARTESIAN_POINT('Origin',(28.9728913804021,-7.84863759081066E-16,
0.));
#15712=CARTESIAN_POINT('Origin',(30.4110679337117,0.,0.));
#15713=CARTESIAN_POINT('Origin',(28.9729800631879,0.,0.));
#15714=CARTESIAN_POINT('',(28.6729800631879,-7.48124356711879E-16,6.1088989677085));
#15715=CARTESIAN_POINT('Origin',(28.9729800631879,-7.48124356711878E-16,
6.1088989677085));
#15716=CARTESIAN_POINT('Origin',(28.6729800631879,0.,0.));
#15717=CARTESIAN_POINT('Origin',(28.6729800631879,0.,-6.40881029802658));
#27692=UNCERTAINTY_MEASURE_WITH_UNIT(LENGTH_MEASURE(0.01),#27708,
'DISTANCE_ACCURACY_VALUE',
'Maximum model space distance between geometric entities at asserted c
onnectivities');
#27695=UNCERTAINTY_MEASURE_WITH_UNIT(LENGTH_MEASURE(0.01),#27708,
'DISTANCE_ACCURACY_VALUE',
'Maximum model space distance between geometric entities at asserted c
onnectivities');
#27704=(
GEOMETRIC_REPRESENTATION_CONTEXT(3)
GLOBAL_UNCERTAINTY_ASSIGNED_CONTEXT((#27692))
GLOBAL_UNIT_ASSIGNED_CONTEXT((#27708,#27710,#27711))
REPRESENTATION_CONTEXT('','3D')
);
#27707=(
GEOMETRIC_REPRESENTATION_CONTEXT(3)
GLOBAL_UNCERTAINTY_ASSIGNED_CONTEXT((#27695))
GLOBAL_UNIT_ASSIGNED_CONTEXT((#27708,#27710,#27711))
REPRESENTATION_CONTEXT('','3D')
);
#27708=(
LENGTH_UNIT()
NAMED_UNIT(*)
SI_UNIT(.MILLI.,.METRE.)
);
#27710=(
NAMED_UNIT(*)
PLANE_ANGLE_UNIT()
SI_UNIT($,.RADIAN.)
);
#27711=(
NAMED_UNIT(*)
SI_UNIT($,.STERADIAN.)
SOLID_ANGLE_UNIT()
);
#27720=SHAPE_DEFINITION_REPRESENTATION(#27731,#27752);
#27731=PRODUCT_DEFINITION_SHAPE('',$,#27764);
#27752=SHAPE_REPRESENTATION('',(#4144),#27704);
#27755=PRODUCT_DEFINITION_CONTEXT('part definition',#27790,'design');
#27764=PRODUCT_DEFINITION('Ring_02','Ring_02',#27775,#27755);
#27775=PRODUCT_DEFINITION_FORMATION('',$,#27800);
#27790=APPLICATION_CONTEXT(
'Core Data for Automotive Mechanical Design Process');
#27791=PRODUCT_CONTEXT('part definition',#27790,'mechanical');
#27800=PRODUCT('Ring_02','Ring_02',$,(#27791));
#27804=PRESENTATION_STYLE_ASSIGNMENT((#27806));
#27806=SURFACE_STYLE_USAGE(.BOTH.,#27808);
#27808=SURFACE_SIDE_STYLE('',(#27810));
#27810=SURFACE_STYLE_FILL_AREA(#27812);
#27812=FILL_AREA_STYLE('Opaque(160,160,160)',(#27814));
#27814=FILL_AREA_STYLE_COLOUR('Opaque(160,160,160)',#27816);
#27816=COLOUR_RGB('Opaque(160,160,160)', 0.09019608, 0.27058824, 0.51372549);
ENDSEC;
END-ISO-10303-21;
